ISO-10303-21;
HEADER;
FILE_DESCRIPTION (('STEP AP214'),
    '1' );
FILE_NAME ('socket head cap screw_iso_ISO 4762 M5 x 50 - 22N.step',
    '2026-10-02T06:35:35',
    ( '' ),
    ( '' ),
    'SwSTEP 2.0',
    'SolidWorks 2026',
    '' );
FILE_SCHEMA (( 'AUTOMOTIVE_DESIGN' ));
ENDSEC;

DATA;
#1=ORIENTED_EDGE ( 'NONE', *, *, #7352, .F. ) ;
#9=CARTESIAN_POINT ( 'NONE',  ( 2.500000000000002220, -1.178949249685208533, 2.042000000000002036 ) ) ;
#17=CARTESIAN_POINT ( 'NONE',  ( 54.55500000000000682, 0.000000000000000000, 0.000000000000000000 ) ) ;
#23=VERTEX_POINT ( 'NONE', #4041 ) ;
#24=ADVANCED_FACE ( 'NONE', ( #13370 ), #10311, .T. ) ;
#35=AXIS2_PLACEMENT_3D ( 'NONE', #9136, #13779, #7988 ) ;
#44=ORIENTED_EDGE ( 'NONE', *, *, #3478, .T. ) ;
#89=CIRCLE ( 'NONE', #12700, 0.2000000000000000944 ) ;
#91=EDGE_CURVE ( 'NONE', #7570, #11525, #4401, .T. ) ;
#95=DIRECTION ( 'NONE',  ( 1.000000000000000000, 0.000000000000000000, 0.000000000000000000 ) ) ;
#121=AXIS2_PLACEMENT_3D ( 'NONE', #1011, #8960, #6603 ) ;
#126=ORIENTED_EDGE ( 'NONE', *, *, #9552, .T. ) ;
#159=CARTESIAN_POINT ( 'NONE',  ( 2.500000000000002220, 0.000000000000000000, 0.000000000000000000 ) ) ;
#161=CARTESIAN_POINT ( 'NONE',  ( 2.500000000000002220, -1.178949249685208533, 2.042000000000002036 ) ) ;
#210=CARTESIAN_POINT ( 'NONE',  ( 0.2500000000000002220, 0.000000000000000000, 4.250000000000000000 ) ) ;
#265=CARTESIAN_POINT ( 'NONE',  ( 2.500000000000002220, -2.357898499370437939, 0.000000000000000000 ) ) ;
#274=FACE_BOUND ( 'NONE', #10845, .T. ) ;
#277=CARTESIAN_POINT ( 'NONE',  ( 0.000000000000000000, -2.357898499370437939, 0.000000000000000000 ) ) ;
#290=ORIENTED_EDGE ( 'NONE', *, *, #1074, .T. ) ;
#296=CARTESIAN_POINT ( 'NONE',  ( 0.000000000000000000, 0.000000000000000000, 0.000000000000000000 ) ) ;
#300=EDGE_LOOP ( 'NONE', ( #5220, #1476, #5090, #12913, #8527, #13334 ) ) ;
#307=ORIENTED_EDGE ( 'NONE', *, *, #3478, .F. ) ;
#422=EDGE_LOOP ( 'NONE', ( #2628, #5228, #14534, #2063, #11947 ) ) ;
#427=PRESENTATION_STYLE_ASSIGNMENT (( #6185 ) ) ;
#454=CARTESIAN_POINT ( 'NONE',  ( 0.2500000000000002220, 0.000000000000000000, 0.000000000000000000 ) ) ;
#471=MECHANICAL_DESIGN_GEOMETRIC_PRESENTATION_REPRESENTATION('',(#9665),#12840);
#485=EDGE_CURVE ( 'NONE', #13764, #628, #7706, .T. ) ;
#513=AXIS2_PLACEMENT_3D ( 'NONE', #2469, #8396, #7236 ) ;
#541=VECTOR ( 'NONE', #6175, 1000.000000000000114 ) ;
#560=CARTESIAN_POINT ( 'NONE',  ( 0.000000000000000000, 1.178949249685208533, -2.042000000000002036 ) ) ;
#570=TOROIDAL_SURFACE ( 'NONE', #4222, 4.000000000000000000, 0.2500000000000000000 ) ;
#625=CARTESIAN_POINT ( 'NONE',  ( 2.500000000000002220, 2.357898499370430834, -6.938893903907228378E-15 ) ) ;
#628=VERTEX_POINT ( 'NONE', #10436 ) ;
#635=CARTESIAN_POINT ( 'NONE',  ( 5.000000000000007994, 0.000000000000000000, 2.775557561562891351E-14 ) ) ;
#661=EDGE_LOOP ( 'NONE', ( #9242, #12653, #10598, #12423, #14869 ) ) ;
#676=CARTESIAN_POINT ( 'NONE',  ( 0.000000000000000000, -1.178949249685208533, 2.042000000000002036 ) ) ;
#692=ORIENTED_EDGE ( 'NONE', *, *, #8053, .F. ) ;
#694=EDGE_CURVE ( 'NONE', #12241, #13116, #2321, .T. ) ;
#715=DIRECTION ( 'NONE',  ( 0.000000000000000000, 0.4999999999999995559, -0.8660254037844389297 ) ) ;
#756=AXIS2_PLACEMENT_3D ( 'NONE', #6672, #13513, #11168 ) ;
#776=EDGE_LOOP ( 'NONE', ( #8992, #2169, #9336, #8022 ) ) ;
#821=ORIENTED_EDGE ( 'NONE', *, *, #12506, .T. ) ;
#847=DIRECTION ( 'NONE',  ( 0.000000000000000000, 0.5000000000000012212, 0.8660254037844380415 ) ) ;
#889=CARTESIAN_POINT ( 'NONE',  ( 0.2500000000000002220, 0.000000000000000000, 0.000000000000000000 ) ) ;
#905=DIRECTION ( 'NONE',  ( 0.000000000000000000, 0.000000000000000000, 1.000000000000000000 ) ) ;
#919=CARTESIAN_POINT ( 'NONE',  ( 2.500000000000002220, 0.000000000000000000, 0.000000000000000000 ) ) ;
#929=DIRECTION ( 'NONE',  ( 0.000000000000000000, -1.000000000000000000, 1.471414886128460880E-15 ) ) ;
#963=CARTESIAN_POINT ( 'NONE',  ( 5.000000000000004441, 0.000000000000000000, 2.775557561562891351E-14 ) ) ;
#972=LINE ( 'NONE', #676, #11811 ) ;
#973=AXIS2_PLACEMENT_3D ( 'NONE', #11244, #6440, #847 ) ;
#975=ORIENTED_EDGE ( 'NONE', *, *, #11787, .T. ) ;
#1011=CARTESIAN_POINT ( 'NONE',  ( -31.74999999999995737, 0.000000000000000000, -2.775557561562891351E-14 ) ) ;
#1058=ORIENTED_EDGE ( 'NONE', *, *, #12704, .T. ) ;
#1074=EDGE_CURVE ( 'NONE', #11288, #23, #6852, .T. ) ;
#1081=DIRECTION ( 'NONE',  ( 0.000000000000000000, -0.5000000000000008882, -0.8660254037844380415 ) ) ;
#1133=( NAMED_UNIT ( * ) SI_UNIT ( $, .STERADIAN. ) SOLID_ANGLE_UNIT ( ) );
#1160=CARTESIAN_POINT ( 'NONE',  ( 2.500000000000002220, 2.357898499370430834, -6.938893903907228378E-15 ) ) ;
#1190=PLANE ( 'NONE',  #2216 ) ;
#1208=PLANE ( 'NONE',  #14822 ) ;
#1259=CARTESIAN_POINT ( 'NONE',  ( 2.500000000000002220, 2.357898499370430834, -6.938893903907228378E-15 ) ) ;
#1267=FACE_OUTER_BOUND ( 'NONE', #14581, .T. ) ;
#1285=AXIS2_PLACEMENT_3D ( 'NONE', #963, #8998, #5583 ) ;
#1298=ORIENTED_EDGE ( 'NONE', *, *, #2210, .F. ) ;
#1303=AXIS2_PLACEMENT_3D ( 'NONE', #10832, #10985, #4009 ) ;
#1306=DIRECTION ( 'NONE',  ( -1.000000000000000000, 0.000000000000000000, 0.000000000000000000 ) ) ;
#1322=LINE ( 'NONE', #2374, #2219 ) ;
#1336=LINE ( 'NONE', #4756, #9747 ) ;
#1345=AXIS2_PLACEMENT_3D ( 'NONE', #4265, #12374, #12307 ) ;
#1347=DIRECTION ( 'NONE',  ( 1.000000000000000000, 0.000000000000000000, 0.000000000000000000 ) ) ;
#1353=ADVANCED_FACE ( 'NONE', ( #5253 ), #5402, .F. ) ;
#1414=DIRECTION ( 'NONE',  ( 0.000000000000000000, 0.000000000000000000, -1.000000000000000000 ) ) ;
#1422=CARTESIAN_POINT ( 'NONE',  ( 55.00000000000000711, 0.000000000000000000, 2.055000000000000160 ) ) ;
#1442=APPLICATION_CONTEXT ( 'automotive_design' ) ;
#1463=LINE ( 'NONE', #11869, #7105 ) ;
#1474=EDGE_CURVE ( 'NONE', #3015, #13429, #11565, .T. ) ;
#1476=ORIENTED_EDGE ( 'NONE', *, *, #11787, .F. ) ;
#1491=AXIS2_PLACEMENT_3D ( 'NONE', #919, #5537, #12679 ) ;
#1523=CARTESIAN_POINT ( 'NONE',  ( 0.000000000000000000, -2.357898499370437939, 0.000000000000000000 ) ) ;
#1531=CIRCLE ( 'NONE', #11482, 2.500000000000000444 ) ;
#1563=EDGE_CURVE ( 'NONE', #13020, #12128, #972, .T. ) ;
#1636=UNCERTAINTY_MEASURE_WITH_UNIT (LENGTH_MEASURE( 1.000000000000000082E-05 ), #12959, 'distance_accuracy_value', 'NONE');
#1680=PLANE ( 'NONE',  #9851 ) ;
#1699=CONICAL_SURFACE ( 'NONE', #4377, 2.055000000000000160, 0.7853981633974479459 ) ;
#1709=DIRECTION ( 'NONE',  ( 0.000000000000000000, 1.000000000000000000, 1.224646799147353207E-16 ) ) ;
#1712=DIRECTION ( 'NONE',  ( 1.000000000000000000, 0.000000000000000000, 0.000000000000000000 ) ) ;
#1776=CARTESIAN_POINT ( 'NONE',  ( 0.000000000000000000, 2.357898499370430834, 0.000000000000000000 ) ) ;
#1783=CARTESIAN_POINT ( 'NONE',  ( 2.500000000000002220, -2.357898499370437939, 0.000000000000000000 ) ) ;
#1795=ORIENTED_EDGE ( 'NONE', *, *, #14510, .F. ) ;
#1818=VECTOR ( 'NONE', #8430, 1000.000000000000000 ) ;
#1825=AXIS2_PLACEMENT_3D ( 'NONE', #13067, #6214, #11940 ) ;
#1826=FACE_OUTER_BOUND ( 'NONE', #422, .T. ) ;
#1864=DIRECTION ( 'NONE',  ( -1.000000000000000000, 0.000000000000000000, 0.000000000000000000 ) ) ;
#1884=CARTESIAN_POINT ( 'NONE',  ( 55.00000000000000711, 0.000000000000000000, 0.000000000000000000 ) ) ;
#1896=DIRECTION ( 'NONE',  ( 0.000000000000000000, 0.000000000000000000, 1.000000000000000000 ) ) ;
#1929=DIRECTION ( 'NONE',  ( 0.000000000000000000, 0.000000000000000000, 1.000000000000000000 ) ) ;
#1946=EDGE_LOOP ( 'NONE', ( #6602, #8176, #12056, #2754, #6989 ) ) ;
#1950=VECTOR ( 'NONE', #5524, 1000.000000000000000 ) ;
#1986=ORIENTED_EDGE ( 'NONE', *, *, #7871, .F. ) ;
#2052=CIRCLE ( 'NONE', #8828, 2.041999999999999815 ) ;
#2054=PLANE ( 'NONE',  #11174 ) ;
#2063=ORIENTED_EDGE ( 'NONE', *, *, #13768, .F. ) ;
#2077=CIRCLE ( 'NONE', #14932, 2.500000000000000444 ) ;
#2078=CARTESIAN_POINT ( 'NONE',  ( 5.200000000000006395, 0.000000000000000000, 2.775557561562891351E-14 ) ) ;
#2081=ORIENTED_EDGE ( 'NONE', *, *, #9552, .F. ) ;
#2113=CARTESIAN_POINT ( 'NONE',  ( -31.74999999999995737, 0.000000000000000000, -2.775557561562891351E-14 ) ) ;
#2123=DIRECTION ( 'NONE',  ( 0.000000000000000000, 0.000000000000000000, 1.000000000000000000 ) ) ;
#2139=CARTESIAN_POINT ( 'NONE',  ( -31.74999999999995737, 0.000000000000000000, 2.499999999999972911 ) ) ;
#2169=ORIENTED_EDGE ( 'NONE', *, *, #12047, .T. ) ;
#2173=DIRECTION ( 'NONE',  ( 0.000000000000000000, 0.000000000000000000, 1.000000000000000000 ) ) ;
#2196=CIRCLE ( 'NONE', #7312, 2.700000000000000622 ) ;
#2210=EDGE_CURVE ( 'NONE', #5057, #14819, #14015, .T. ) ;
#2216=AXIS2_PLACEMENT_3D ( 'NONE', #12738, #2329, #1414 ) ;
#2219=VECTOR ( 'NONE', #3531, 999.9999999999998863 ) ;
#2240=DIRECTION ( 'NONE',  ( 0.000000000000000000, -0.4999999999999997780, 0.8660254037844388186 ) ) ;
#2243=EDGE_LOOP ( 'NONE', ( #1298, #12351, #3364, #10250, #9546 ) ) ;
#2257=( NAMED_UNIT ( * ) PLANE_ANGLE_UNIT ( ) SI_UNIT ( $, .RADIAN. ) );
#2265=DIRECTION ( 'NONE',  ( 0.000000000000000000, 0.000000000000000000, 1.000000000000000000 ) ) ;
#2284=AXIS2_PLACEMENT_3D ( 'NONE', #6292, #14222, #2601 ) ;
#2321=LINE ( 'NONE', #1259, #7864 ) ;
#2329=DIRECTION ( 'NONE',  ( 1.000000000000000000, 0.000000000000000000, 0.000000000000000000 ) ) ;
#2340=CARTESIAN_POINT ( 'NONE',  ( 2.500000000000002220, 0.000000000000000000, 0.000000000000000000 ) ) ;
#2344=CARTESIAN_POINT ( 'NONE',  ( 2.500000000000002220, 2.357898499370430834, -6.938893903907228378E-15 ) ) ;
#2374=CARTESIAN_POINT ( 'NONE',  ( 55.00000000000000711, 2.516649172247811061E-16, -2.055000000000000160 ) ) ;
#2400=CIRCLE ( 'NONE', #11864, 2.055000000000000160 ) ;
#2410=CARTESIAN_POINT ( 'NONE',  ( 2.500000000000002220, 2.357898499370430834, -6.938893903907228378E-15 ) ) ;
#2444=TOROIDAL_SURFACE ( 'NONE', #513, 2.700000000000000622, 0.2000000000000000111 ) ;
#2469=CARTESIAN_POINT ( 'NONE',  ( 5.200000000000006395, 0.000000000000000000, 2.775557561562891351E-14 ) ) ;
#2473=DIRECTION ( 'NONE',  ( 0.000000000000000000, -0.5000000000000012212, -0.8660254037844380415 ) ) ;
#2474=VERTEX_POINT ( 'NONE', #5778 ) ;
#2506=ORIENTED_EDGE ( 'NONE', *, *, #14971, .F. ) ;
#2508=CIRCLE ( 'NONE', #1285, 2.700000000000000622 ) ;
#2543=DIRECTION ( 'NONE',  ( 0.000000000000000000, 0.000000000000000000, 1.000000000000000000 ) ) ;
#2545=EDGE_CURVE ( 'NONE', #14464, #13630, #10827, .T. ) ;
#2584=CARTESIAN_POINT ( 'NONE',  ( 2.500000000000002220, 2.357898499370430834, -6.938893903907228378E-15 ) ) ;
#2588=DIRECTION ( 'NONE',  ( 0.000000000000000000, 0.4999999999999997780, -0.8660254037844387076 ) ) ;
#2594=VERTEX_POINT ( 'NONE', #5714 ) ;
#2601=DIRECTION ( 'NONE',  ( 0.000000000000000000, 0.000000000000000000, 1.000000000000000000 ) ) ;
#2611=VECTOR ( 'NONE', #3402, 1000.000000000000000 ) ;
#2617=EDGE_LOOP ( 'NONE', ( #821, #14798, #4546 ) ) ;
#2621=EDGE_LOOP ( 'NONE', ( #13318, #126, #7456, #6714 ) ) ;
#2628=ORIENTED_EDGE ( 'NONE', *, *, #8795, .T. ) ;
#2648=EDGE_LOOP ( 'NONE', ( #8451, #9909, #3886 ) ) ;
#2650=LINE ( 'NONE', #8637, #12132 ) ;
#2659=LINE ( 'NONE', #12082, #8017 ) ;
#2672=ADVANCED_FACE ( 'NONE', ( #7289 ), #4737, .F. ) ;
#2688=CARTESIAN_POINT ( 'NONE',  ( 0.000000000000000000, 1.178949249685208533, -2.042000000000002036 ) ) ;
#2690=ORIENTED_EDGE ( 'NONE', *, *, #13768, .T. ) ;
#2730=ORIENTED_EDGE ( 'NONE', *, *, #13517, .F. ) ;
#2754=ORIENTED_EDGE ( 'NONE', *, *, #9125, .F. ) ;
#2777=ADVANCED_FACE ( 'NONE', ( #7591 ), #1680, .F. ) ;
#2802=EDGE_LOOP ( 'NONE', ( #5915, #4773, #8392, #11552 ) ) ;
#2839=CARTESIAN_POINT ( 'NONE',  ( 55.00000000000000711, 0.000000000000000000, 2.055000000000000160 ) ) ;
#2850=PLANE ( 'NONE',  #11939 ) ;
#2887=DIRECTION ( 'NONE',  ( 0.000000000000000000, 0.000000000000000000, -1.000000000000000000 ) ) ;
#2895=COLOUR_RGB ( '', 0.72549020, 0.75294118, 0.79215686) ;
#2924=VECTOR ( 'NONE', #10337, 1000.000000000000227 ) ;
#2958=FACE_OUTER_BOUND ( 'NONE', #776, .T. ) ;
#2961=CARTESIAN_POINT ( 'NONE',  ( -31.74999999999995737, 5.204748896376250699E-16, -4.250000000000028422 ) ) ;
#2987=CIRCLE ( 'NONE', #9752, 0.2000000000000000944 ) ;
#2997=ORIENTED_EDGE ( 'NONE', *, *, #3752, .F. ) ;
#3013=EDGE_CURVE ( 'NONE', #11582, #9151, #6359, .T. ) ;
#3015=VERTEX_POINT ( 'NONE', #5061 ) ;
#3035=VECTOR ( 'NONE', #4382, 1000.000000000000000 ) ;
#3046=FACE_OUTER_BOUND ( 'NONE', #11594, .T. ) ;
#3095=ORIENTED_EDGE ( 'NONE', *, *, #7352, .T. ) ;
#3118=DIRECTION ( 'NONE',  ( -1.000000000000000000, 0.000000000000000000, 0.000000000000000000 ) ) ;
#3165=AXIS2_PLACEMENT_3D ( 'NONE', #5686, #3416, #8040 ) ;
#3179=ORIENTED_EDGE ( 'NONE', *, *, #13517, .T. ) ;
#3195=FACE_OUTER_BOUND ( 'NONE', #2617, .T. ) ;
#3219=LINE ( 'NONE', #1783, #9026 ) ;
#3225=EDGE_CURVE ( 'NONE', #9151, #5320, #10274, .T. ) ;
#3245=EDGE_CURVE ( 'NONE', #5022, #11082, #2508, .T. ) ;
#3257=ORIENTED_EDGE ( 'NONE', *, *, #11318, .F. ) ;
#3260=VECTOR ( 'NONE', #3652, 1000.000000000000114 ) ;
#3304=CONICAL_SURFACE ( 'NONE', #4031, 2.041999999999999815, 1.047197551196591858 ) ;
#3309=LINE ( 'NONE', #7928, #13193 ) ;
#3312=ORIENTED_EDGE ( 'NONE', *, *, #11427, .F. ) ;
#3364=ORIENTED_EDGE ( 'NONE', *, *, #11977, .T. ) ;
#3371=AXIS2_PLACEMENT_3D ( 'NONE', #4104, #3118, #1896 ) ;
#3385=EDGE_CURVE ( 'NONE', #4050, #13764, #1336, .T. ) ;
#3402=DIRECTION ( 'NONE',  ( -1.000000000000000000, 0.000000000000000000, 0.000000000000000000 ) ) ;
#3416=DIRECTION ( 'NONE',  ( 0.000000000000000000, 0.8660254037844381525, -0.5000000000000008882 ) ) ;
#3440=DIRECTION ( 'NONE',  ( -1.000000000000000000, 0.000000000000000000, 0.000000000000000000 ) ) ;
#3444=CARTESIAN_POINT ( 'NONE',  ( 5.200000000000006395, 0.000000000000000000, 2.775557561562891351E-14 ) ) ;
#3453=MECHANICAL_DESIGN_GEOMETRIC_PRESENTATION_REPRESENTATION('',(#8495),#12388);
#3478=EDGE_CURVE ( 'NONE', #14961, #7570, #11668, .T. ) ;
#3491=DIRECTION ( 'NONE',  ( 0.000000000000000000, 0.000000000000000000, 1.000000000000000000 ) ) ;
#3492=LINE ( 'NONE', #2344, #3695 ) ;
#3531=DIRECTION ( 'NONE',  ( -0.7071067811865479058, 8.659560562354930393E-17, -0.7071067811865472397 ) ) ;
#3539=AXIS2_PLACEMENT_3D ( 'NONE', #454, #5084, #14349 ) ;
#3592=DIRECTION ( 'NONE',  ( 0.000000000000000000, -1.287488025362403787E-15, -1.000000000000000000 ) ) ;
#3609=ORIENTED_EDGE ( 'NONE', *, *, #12540, .T. ) ;
#3620=EDGE_CURVE ( 'NONE', #8108, #12802, #5400, .T. ) ;
#3643=PRESENTATION_STYLE_ASSIGNMENT (( #9332 ) ) ;
#3652=DIRECTION ( 'NONE',  ( 0.000000000000000000, -0.4999999999999997780, 0.8660254037844388186 ) ) ;
#3658=AXIS2_PLACEMENT_3D ( 'NONE', #7749, #12396, #13381 ) ;
#3695=VECTOR ( 'NONE', #6961, 999.9999999999998863 ) ;
#3736=PLANE ( 'NONE',  #9333 ) ;
#3752=EDGE_CURVE ( 'NONE', #13429, #14961, #3219, .T. ) ;
#3754=AXIS2_PLACEMENT_3D ( 'NONE', #8858, #6338, #905 ) ;
#3847=SURFACE_STYLE_FILL_AREA ( #9447 ) ;
#3886=ORIENTED_EDGE ( 'NONE', *, *, #11325, .F. ) ;
#3895=EDGE_CURVE ( 'NONE', #13630, #14464, #1531, .T. ) ;
#3911=DIRECTION ( 'NONE',  ( -0.5000000000000051070, 1.060575238724903217E-16, -0.8660254037844355990 ) ) ;
#4009=DIRECTION ( 'NONE',  ( 0.000000000000000000, 0.000000000000000000, -1.000000000000000000 ) ) ;
#4011=ORIENTED_EDGE ( 'NONE', *, *, #5838, .T. ) ;
#4031=AXIS2_PLACEMENT_3D ( 'NONE', #2340, #11763, #4775 ) ;
#4039=CARTESIAN_POINT ( 'NONE',  ( 2.500000000000002220, 0.000000000000000000, 2.041999999999999815 ) ) ;
#4041=CARTESIAN_POINT ( 'NONE',  ( 54.55500000000000682, 0.000000000000000000, 2.500000000000000444 ) ) ;
#4050=VERTEX_POINT ( 'NONE', #5032 ) ;
#4090=FACE_OUTER_BOUND ( 'NONE', #7803, .T. ) ;
#4104=CARTESIAN_POINT ( 'NONE',  ( 2.500000000000002220, 0.000000000000000000, 0.000000000000000000 ) ) ;
#4123=CARTESIAN_POINT ( 'NONE',  ( -31.74999999999995737, 0.000000000000000000, -2.775557561562891351E-14 ) ) ;
#4142=EDGE_LOOP ( 'NONE', ( #4944, #2690, #4270 ) ) ;
#4147=COLOUR_RGB ( '', 0.72549020, 0.75294118, 0.79215686) ;
#4153=EDGE_LOOP ( 'NONE', ( #12525, #14322, #3609, #13501 ) ) ;
#4171=CARTESIAN_POINT ( 'NONE',  ( 0.000000000000000000, -1.178949249685208533, 2.042000000000002036 ) ) ;
#4197=DIRECTION ( 'NONE',  ( 0.000000000000000000, 1.471414886128460880E-15, 1.000000000000000000 ) ) ;
#4222=AXIS2_PLACEMENT_3D ( 'NONE', #889, #10130, #10974 ) ;
#4230=EDGE_LOOP ( 'NONE', ( #5728, #3179, #3312, #11314 ) ) ;
#4265=CARTESIAN_POINT ( 'NONE',  ( 2.500000000000002220, 2.357898499370430834, -6.938893903907228378E-15 ) ) ;
#4270=ORIENTED_EDGE ( 'NONE', *, *, #5483, .F. ) ;
#4285=FACE_OUTER_BOUND ( 'NONE', #2621, .T. ) ;
#4315=ORIENTED_EDGE ( 'NONE', *, *, #91, .T. ) ;
#4337=CARTESIAN_POINT ( 'NONE',  ( 2.500000000000002220, 1.178949249685208533, -2.042000000000002036 ) ) ;
#4377=AXIS2_PLACEMENT_3D ( 'NONE', #1884, #12219, #14575 ) ;
#4382=DIRECTION ( 'NONE',  ( 0.000000000000000000, 1.000000000000000000, -1.471414886128460880E-15 ) ) ;
#4383=VECTOR ( 'NONE', #8059, 1000.000000000000000 ) ;
#4401=LINE ( 'NONE', #9011, #2611 ) ;
#4415=CARTESIAN_POINT ( 'NONE',  ( 2.500000000000002220, -1.768423874527823347, -1.021000000000001018 ) ) ;
#4445=CARTESIAN_POINT ( 'NONE',  ( 2.500000000000002220, -2.357898499370437939, 0.000000000000000000 ) ) ;
#4520=ORIENTED_EDGE ( 'NONE', *, *, #3225, .T. ) ;
#4522=PLANE ( 'NONE',  #35 ) ;
#4542=CYLINDRICAL_SURFACE ( 'NONE', #7041, 2.500000000000000444 ) ;
#4546=ORIENTED_EDGE ( 'NONE', *, *, #7537, .F. ) ;
#4576=CARTESIAN_POINT ( 'NONE',  ( 2.500000000000002220, -2.357898499370437939, 0.000000000000000000 ) ) ;
#4656=DIRECTION ( 'NONE',  ( 0.000000000000000000, 0.000000000000000000, -1.000000000000000000 ) ) ;
#4662=ORIENTED_EDGE ( 'NONE', *, *, #13578, .F. ) ;
#4693=ADVANCED_FACE ( 'NONE', ( #12896 ), #3304, .F. ) ;
#4737=PLANE ( 'NONE',  #9366 ) ;
#4756=CARTESIAN_POINT ( 'NONE',  ( 2.500000000000002220, -1.178949249685208533, 2.042000000000002036 ) ) ;
#4773=ORIENTED_EDGE ( 'NONE', *, *, #13256, .T. ) ;
#4775=DIRECTION ( 'NONE',  ( 0.000000000000000000, 0.000000000000000000, 1.000000000000000000 ) ) ;
#4777=DIRECTION ( 'NONE',  ( -1.000000000000000000, 0.000000000000000000, 0.000000000000000000 ) ) ;
#4819=CARTESIAN_POINT ( 'NONE',  ( 2.500000000000002220, 2.500728763858895382E-16, -2.041999999999999815 ) ) ;
#4821=DIRECTION ( 'NONE',  ( -1.000000000000000000, 0.000000000000000000, 0.000000000000000000 ) ) ;
#4896=LINE ( 'NONE', #9507, #14340 ) ;
#4897=DIRECTION ( 'NONE',  ( 0.000000000000000000, -1.000000000000000000, 0.000000000000000000 ) ) ;
#4944=ORIENTED_EDGE ( 'NONE', *, *, #5559, .F. ) ;
#4956=LINE ( 'NONE', #4039, #8729 ) ;
#4958=VECTOR ( 'NONE', #7522, 1000.000000000000000 ) ;
#5004=EDGE_LOOP ( 'NONE', ( #14853, #1986, #11655, #44, #4315 ) ) ;
#5022=VERTEX_POINT ( 'NONE', #10497 ) ;
#5032=CARTESIAN_POINT ( 'NONE',  ( 2.500000000000002220, -1.178949249685208533, 2.042000000000002036 ) ) ;
#5057=VERTEX_POINT ( 'NONE', #6762 ) ;
#5061=CARTESIAN_POINT ( 'NONE',  ( 2.500000000000002220, -1.768423874527823347, 1.021000000000001018 ) ) ;
#5083=EDGE_CURVE ( 'NONE', #6523, #628, #1463, .T. ) ;
#5084=DIRECTION ( 'NONE',  ( 1.000000000000000000, -0.000000000000000000, -0.000000000000000000 ) ) ;
#5090=ORIENTED_EDGE ( 'NONE', *, *, #1563, .T. ) ;
#5107=ADVANCED_FACE ( 'NONE', ( #7294 ), #6146, .T. ) ;
#5108=AXIS2_PLACEMENT_3D ( 'NONE', #296, #6125, #10768 ) ;
#5123=PRODUCT ( 'socket head cap screw_iso_ISO 4762 M5 x 50 - 22N', 'socket head cap screw_iso_ISO 4762 M5 x 50 - 22N', '', ( #5282 ) ) ;
#5146=ORIENTED_EDGE ( 'NONE', *, *, #5083, .T. ) ;
#5161=ORIENTED_EDGE ( 'NONE', *, *, #485, .F. ) ;
#5208=CARTESIAN_POINT ( 'NONE',  ( 2.500000000000002220, 2.357898499370430834, -6.938893903907228378E-15 ) ) ;
#5220=ORIENTED_EDGE ( 'NONE', *, *, #7408, .T. ) ;
#5228=ORIENTED_EDGE ( 'NONE', *, *, #8091, .F. ) ;
#5245=FACE_OUTER_BOUND ( 'NONE', #8518, .T. ) ;
#5249=VECTOR ( 'NONE', #3911, 1000.000000000000114 ) ;
#5253=FACE_OUTER_BOUND ( 'NONE', #14034, .T. ) ;
#5282=PRODUCT_CONTEXT ( 'NONE', #1442, 'mechanical' ) ;
#5287=DIRECTION ( 'NONE',  ( 0.000000000000000000, 0.000000000000000000, 1.000000000000000000 ) ) ;
#5320=VERTEX_POINT ( 'NONE', #7675 ) ;
#5342=FILL_AREA_STYLE ('',( #9180 ) ) ;
#5400=CIRCLE ( 'NONE', #11223, 2.055000000000000160 ) ;
#5402=PLANE ( 'NONE',  #7517 ) ;
#5417=AXIS2_PLACEMENT_3D ( 'NONE', #17, #7982, #12848 ) ;
#5434=ORIENTED_EDGE ( 'NONE', *, *, #10092, .T. ) ;
#5441=VECTOR ( 'NONE', #10145, 1000.000000000000000 ) ;
#5451=TOROIDAL_SURFACE ( 'NONE', #3754, 4.000000000000000000, 0.2500000000000000000 ) ;
#5473=EDGE_CURVE ( 'NONE', #12128, #11525, #14902, .T. ) ;
#5475=ORIENTED_EDGE ( 'NONE', *, *, #1474, .F. ) ;
#5476=DIRECTION ( 'NONE',  ( 0.000000000000000000, -0.4999999999999995559, 0.8660254037844389297 ) ) ;
#5483=EDGE_CURVE ( 'NONE', #6523, #2474, #6161, .T. ) ;
#5504=ORIENTED_EDGE ( 'NONE', *, *, #3620, .T. ) ;
#5524=DIRECTION ( 'NONE',  ( -1.000000000000000000, 0.000000000000000000, 0.000000000000000000 ) ) ;
#5530=DIRECTION ( 'NONE',  ( -1.000000000000000000, 0.000000000000000000, 0.000000000000000000 ) ) ;
#5537=DIRECTION ( 'NONE',  ( -1.000000000000000000, 0.000000000000000000, 0.000000000000000000 ) ) ;
#5559=EDGE_CURVE ( 'NONE', #12241, #6523, #10556, .T. ) ;
#5583=DIRECTION ( 'NONE',  ( 0.000000000000000000, 0.000000000000000000, -1.000000000000000000 ) ) ;
#5612=EDGE_CURVE ( 'NONE', #14961, #3015, #2052, .T. ) ;
#5686=CARTESIAN_POINT ( 'NONE',  ( 2.500000000000002220, -1.178949249685208533, 2.042000000000002036 ) ) ;
#5714=CARTESIAN_POINT ( 'NONE',  ( 5.000000000000007994, 5.204748896376217172E-16, -4.249999999999972466 ) ) ;
#5728=ORIENTED_EDGE ( 'NONE', *, *, #8053, .T. ) ;
#5736=ORIENTED_EDGE ( 'NONE', *, *, #1563, .F. ) ;
#5778=CARTESIAN_POINT ( 'NONE',  ( 2.500000000000002220, 1.768423874527823347, -1.021000000000001018 ) ) ;
#5792=EDGE_LOOP ( 'NONE', ( #2997, #5475, #12148 ) ) ;
#5838=EDGE_CURVE ( 'NONE', #12802, #23, #12964, .T. ) ;
#5868=AXIS2_PLACEMENT_3D ( 'NONE', #4123, #8818, #7520 ) ;
#5885=( NAMED_UNIT ( * ) PLANE_ANGLE_UNIT ( ) SI_UNIT ( $, .RADIAN. ) );
#5915=ORIENTED_EDGE ( 'NONE', *, *, #6517, .F. ) ;
#6014=LINE ( 'NONE', #2688, #6136 ) ;
#6030=DIRECTION ( 'NONE',  ( -0.7071067811865479058, 0.000000000000000000, 0.7071067811865472397 ) ) ;
#6049=CARTESIAN_POINT ( 'NONE',  ( 0.2500000000000002220, 5.204748896376234922E-16, -4.250000000000000000 ) ) ;
#6072=DIRECTION ( 'NONE',  ( 0.000000000000000000, -1.000000000000000000, 1.287488025362403787E-15 ) ) ;
#6119=ORIENTED_EDGE ( 'NONE', *, *, #5559, .T. ) ;
#6125=DIRECTION ( 'NONE',  ( 0.000000000000000000, 0.000000000000000000, 1.000000000000000000 ) ) ;
#6126=AXIS2_PLACEMENT_3D ( 'NONE', #6948, #12582, #2173 ) ;
#6136=VECTOR ( 'NONE', #7381, 1000.000000000000000 ) ;
#6146=CONICAL_SURFACE ( 'NONE', #2284, 2.055000000000000160, 0.7853981633974479459 ) ;
#6154=CARTESIAN_POINT ( 'NONE',  ( 2.500000000000002220, 1.178949249685208533, -2.042000000000002036 ) ) ;
#6161=CIRCLE ( 'NONE', #13443, 2.041999999999999815 ) ;
#6168=LINE ( 'NONE', #1776, #10716 ) ;
#6175=DIRECTION ( 'NONE',  ( 0.000000000000000000, 0.4999999999999995559, -0.8660254037844389297 ) ) ;
#6185=SURFACE_STYLE_USAGE ( .BOTH. , #8398 ) ;
#6214=DIRECTION ( 'NONE',  ( -1.000000000000000000, 0.000000000000000000, 0.000000000000000000 ) ) ;
#6234=CARTESIAN_POINT ( 'NONE',  ( 5.200000000000006395, 0.000000000000000000, -2.699999999999972644 ) ) ;
#6292=CARTESIAN_POINT ( 'NONE',  ( 55.00000000000000711, 0.000000000000000000, 0.000000000000000000 ) ) ;
#6318=DIRECTION ( 'NONE',  ( 0.000000000000000000, 0.000000000000000000, -1.000000000000000000 ) ) ;
#6338=DIRECTION ( 'NONE',  ( -1.000000000000000000, 0.000000000000000000, 0.000000000000000000 ) ) ;
#6359=CIRCLE ( 'NONE', #1303, 0.2500000000000002220 ) ;
#6371=AXIS2_PLACEMENT_3D ( 'NONE', #7707, #9992, #5287 ) ;
#6440=DIRECTION ( 'NONE',  ( 0.000000000000000000, 0.8660254037844380415, -0.5000000000000012212 ) ) ;
#6508=LINE ( 'NONE', #4337, #7004 ) ;
#6517=EDGE_CURVE ( 'NONE', #8372, #11582, #9692, .T. ) ;
#6523=VERTEX_POINT ( 'NONE', #7683 ) ;
#6552=ADVANCED_BREP_SHAPE_REPRESENTATION ( '', ( #9343, #5108 ), #10652 ) ;
#6602=ORIENTED_EDGE ( 'NONE', *, *, #12574, .T. ) ;
#6603=DIRECTION ( 'NONE',  ( 0.000000000000000000, 0.000000000000000000, 1.000000000000000000 ) ) ;
#6654=DIRECTION ( 'NONE',  ( 0.000000000000000000, 0.000000000000000000, 1.000000000000000000 ) ) ;
#6665=CARTESIAN_POINT ( 'NONE',  ( 5.200000000000006395, 3.061616997868349122E-16, -2.499999999999972911 ) ) ;
#6669=CIRCLE ( 'NONE', #3539, 4.250000000000000000 ) ;
#6672=CARTESIAN_POINT ( 'NONE',  ( 2.500000000000002220, 2.357898499370430834, -6.938893903907228378E-15 ) ) ;
#6694=DIRECTION ( 'NONE',  ( 0.000000000000000000, 0.000000000000000000, -1.000000000000000000 ) ) ;
#6714=ORIENTED_EDGE ( 'NONE', *, *, #14511, .F. ) ;
#6715=EDGE_CURVE ( 'NONE', #14819, #7570, #2659, .T. ) ;
#6739=DIRECTION ( 'NONE',  ( 0.000000000000000000, 0.8660254037844389297, 0.4999999999999995559 ) ) ;
#6762=CARTESIAN_POINT ( 'NONE',  ( 3.678949249685234957, 0.000000000000000000, 0.000000000000000000 ) ) ;
#6764=FACE_OUTER_BOUND ( 'NONE', #6964, .T. ) ;
#6773=PRODUCT_DEFINITION_FORMATION_WITH_SPECIFIED_SOURCE ( 'ANY', '', #5123, .NOT_KNOWN. ) ;
#6786=AXIS2_PLACEMENT_3D ( 'NONE', #13661, #7886, #11008 ) ;
#6791=AXIS2_PLACEMENT_3D ( 'NONE', #8758, #1709, #10886 ) ;
#6792=DIRECTION ( 'NONE',  ( 0.000000000000000000, 1.000000000000000000, -1.224646799147353207E-16 ) ) ;
#6797=ORIENTED_EDGE ( 'NONE', *, *, #5083, .F. ) ;
#6845=EDGE_CURVE ( 'NONE', #2594, #8372, #12581, .T. ) ;
#6852=CIRCLE ( 'NONE', #5417, 2.500000000000000444 ) ;
#6941=ADVANCED_FACE ( 'NONE', ( #5245 ), #4542, .T. ) ;
#6948=CARTESIAN_POINT ( 'NONE',  ( 2.500000000000002220, 0.000000000000000000, 0.000000000000000000 ) ) ;
#6960=FACE_BOUND ( 'NONE', #300, .T. ) ;
#6961=DIRECTION ( 'NONE',  ( 0.000000000000000000, -0.5000000000000012212, -0.8660254037844380415 ) ) ;
#6964=EDGE_LOOP ( 'NONE', ( #692, #8791 ) ) ;
#6967=( LENGTH_UNIT ( ) NAMED_UNIT ( * ) SI_UNIT ( .MILLI., .METRE. ) );
#6979=CARTESIAN_POINT ( 'NONE',  ( 5.200000000000006395, 0.000000000000000000, 2.500000000000028422 ) ) ;
#6984=ADVANCED_FACE ( 'NONE', ( #274, #1267 ), #1190, .T. ) ;
#6985=DIRECTION ( 'NONE',  ( 1.000000000000000000, 0.000000000000000000, 0.000000000000000000 ) ) ;
#6989=ORIENTED_EDGE ( 'NONE', *, *, #8091, .T. ) ;
#7003=ORIENTED_EDGE ( 'NONE', *, *, #14510, .T. ) ;
#7004=VECTOR ( 'NONE', #12232, 1000.000000000000000 ) ;
#7005=ADVANCED_FACE ( 'NONE', ( #12878 ), #2444, .F. ) ;
#7012=CIRCLE ( 'NONE', #12133, 2.041999999999999815 ) ;
#7040=EDGE_LOOP ( 'NONE', ( #2730, #5504, #4011, #12862 ) ) ;
#7041=AXIS2_PLACEMENT_3D ( 'NONE', #9859, #11453, #14502 ) ;
#7076=ORIENTED_EDGE ( 'NONE', *, *, #694, .F. ) ;
#7096=CARTESIAN_POINT ( 'NONE',  ( 2.500000000000002220, 0.000000000000000000, 0.000000000000000000 ) ) ;
#7105=VECTOR ( 'NONE', #8293, 1000.000000000000114 ) ;
#7110=CARTESIAN_POINT ( 'NONE',  ( 0.000000000000000000, -1.178949249685222522, -2.042000000000002036 ) ) ;
#7166=EDGE_LOOP ( 'NONE', ( #11121, #7076, #6119, #5146, #1058 ) ) ;
#7190=ORIENTED_EDGE ( 'NONE', *, *, #10884, .T. ) ;
#7236=DIRECTION ( 'NONE',  ( 0.000000000000000000, 0.000000000000000000, -1.000000000000000000 ) ) ;
#7240=VERTEX_POINT ( 'NONE', #14472 ) ;
#7289=FACE_OUTER_BOUND ( 'NONE', #1946, .T. ) ;
#7294=FACE_OUTER_BOUND ( 'NONE', #7040, .T. ) ;
#7312=AXIS2_PLACEMENT_3D ( 'NONE', #12380, #14891, #13445 ) ;
#7352=EDGE_CURVE ( 'NONE', #8099, #2594, #13098, .T. ) ;
#7381=DIRECTION ( 'NONE',  ( 0.000000000000000000, -1.000000000000000000, 1.287488025362403787E-15 ) ) ;
#7385=VECTOR ( 'NONE', #6030, 999.9999999999998863 ) ;
#7408=EDGE_CURVE ( 'NONE', #13116, #11806, #4896, .T. ) ;
#7456=ORIENTED_EDGE ( 'NONE', *, *, #3895, .T. ) ;
#7517=AXIS2_PLACEMENT_3D ( 'NONE', #10024, #4197, #929 ) ;
#7520=DIRECTION ( 'NONE',  ( 0.000000000000000000, 0.000000000000000000, 1.000000000000000000 ) ) ;
#7522=DIRECTION ( 'NONE',  ( -1.000000000000000000, 0.000000000000000000, 0.000000000000000000 ) ) ;
#7537=EDGE_CURVE ( 'NONE', #2474, #14819, #7012, .T. ) ;
#7570=VERTEX_POINT ( 'NONE', #10809 ) ;
#7584=CARTESIAN_POINT ( 'NONE',  ( 55.00000000000000711, 2.789133085058097101E-16, -2.055000000000000160 ) ) ;
#7591=FACE_OUTER_BOUND ( 'NONE', #2648, .T. ) ;
#7603=DIRECTION ( 'NONE',  ( 0.000000000000000000, 0.000000000000000000, 1.000000000000000000 ) ) ;
#7664=CARTESIAN_POINT ( 'NONE',  ( 2.500000000000002220, -6.938893903907228378E-15, -2.042000000000002036 ) ) ;
#7675=CARTESIAN_POINT ( 'NONE',  ( 0.000000000000000000, 5.051668046482832750E-16, -4.000000000000000000 ) ) ;
#7683=CARTESIAN_POINT ( 'NONE',  ( 2.500000000000002220, 1.768423874527823347, 1.020999999999994134 ) ) ;
#7701=FACE_OUTER_BOUND ( 'NONE', #2802, .T. ) ;
#7706=LINE ( 'NONE', #12573, #3035 ) ;
#7707=CARTESIAN_POINT ( 'NONE',  ( 0.000000000000000000, 0.000000000000000000, 0.000000000000000000 ) ) ;
#7729=DIRECTION ( 'NONE',  ( -1.000000000000000000, 0.000000000000000000, 0.000000000000000000 ) ) ;
#7732=CARTESIAN_POINT ( 'NONE',  ( 55.00000000000000711, 0.000000000000000000, 0.000000000000000000 ) ) ;
#7749=CARTESIAN_POINT ( 'NONE',  ( 0.2500000000000002220, 0.000000000000000000, 0.000000000000000000 ) ) ;
#7803=EDGE_LOOP ( 'NONE', ( #14258, #13718, #8125, #2506 ) ) ;
#7812=PLANE ( 'NONE',  #756 ) ;
#7864=VECTOR ( 'NONE', #9368, 1000.000000000000000 ) ;
#7871=EDGE_CURVE ( 'NONE', #13429, #12128, #14982, .T. ) ;
#7886=DIRECTION ( 'NONE',  ( 1.000000000000000000, 0.000000000000000000, 0.000000000000000000 ) ) ;
#7890=DIRECTION ( 'NONE',  ( -1.000000000000000000, 0.000000000000000000, 0.000000000000000000 ) ) ;
#7894=ORIENTED_EDGE ( 'NONE', *, *, #2545, .T. ) ;
#7907=LINE ( 'NONE', #2139, #10185 ) ;
#7928=CARTESIAN_POINT ( 'NONE',  ( 2.500000000000002220, 2.357898499370430834, -6.938893903907228378E-15 ) ) ;
#7953=ORIENTED_EDGE ( 'NONE', *, *, #10884, .F. ) ;
#7982=DIRECTION ( 'NONE',  ( -1.000000000000000000, 0.000000000000000000, 0.000000000000000000 ) ) ;
#7988=DIRECTION ( 'NONE',  ( 0.000000000000000000, 0.000000000000000000, -1.000000000000000000 ) ) ;
#8006=SHAPE_REPRESENTATION ( 'socket head cap screw_iso_ISO 4762 M5 x 50 - 22N', ( #5108 ), #10652 ) ;
#8007=DIRECTION ( 'NONE',  ( 0.000000000000000000, 1.000000000000000000, -1.471414886128460880E-15 ) ) ;
#8017=VECTOR ( 'NONE', #14212, 1000.000000000000000 ) ;
#8020=DIRECTION ( 'NONE',  ( 0.000000000000000000, 1.224646799147353207E-16, 1.000000000000000000 ) ) ;
#8022=ORIENTED_EDGE ( 'NONE', *, *, #12540, .F. ) ;
#8040=DIRECTION ( 'NONE',  ( 0.000000000000000000, 0.5000000000000008882, 0.8660254037844381525 ) ) ;
#8051=ADVANCED_FACE ( 'NONE', ( #11091 ), #9908, .F. ) ;
#8053=EDGE_CURVE ( 'NONE', #12802, #8108, #2400, .T. ) ;
#8059=DIRECTION ( 'NONE',  ( -1.000000000000000000, 0.000000000000000000, 0.000000000000000000 ) ) ;
#8091=EDGE_CURVE ( 'NONE', #7240, #8815, #6508, .T. ) ;
#8099=VERTEX_POINT ( 'NONE', #8946 ) ;
#8108=VERTEX_POINT ( 'NONE', #7584 ) ;
#8115=ADVANCED_FACE ( 'NONE', ( #1826 ), #14812, .F. ) ;
#8125=ORIENTED_EDGE ( 'NONE', *, *, #3013, .T. ) ;
#8176=ORIENTED_EDGE ( 'NONE', *, *, #91, .F. ) ;
#8220=VECTOR ( 'NONE', #3440, 1000.000000000000000 ) ;
#8293=DIRECTION ( 'NONE',  ( 0.000000000000000000, -0.4999999999999997780, 0.8660254037844388186 ) ) ;
#8318=SHAPE_REPRESENTATION_RELATIONSHIP ( 'NONE' , 'NONE' ,  #8006, #6552 ) ;
#8372=VERTEX_POINT ( 'NONE', #6049 ) ;
#8382=DIRECTION ( 'NONE',  ( 0.000000000000000000, 0.000000000000000000, -1.000000000000000000 ) ) ;
#8392=ORIENTED_EDGE ( 'NONE', *, *, #3225, .F. ) ;
#8396=DIRECTION ( 'NONE',  ( 1.000000000000000000, 0.000000000000000000, 0.000000000000000000 ) ) ;
#8398=SURFACE_SIDE_STYLE ('',( #3847 ) ) ;
#8418=DIRECTION ( 'NONE',  ( 0.000000000000000000, 0.000000000000000000, -1.000000000000000000 ) ) ;
#8422=DIRECTION ( 'NONE',  ( -1.000000000000000000, 0.000000000000000000, 0.000000000000000000 ) ) ;
#8430=DIRECTION ( 'NONE',  ( -1.000000000000000000, 0.000000000000000000, 0.000000000000000000 ) ) ;
#8451=ORIENTED_EDGE ( 'NONE', *, *, #10092, .F. ) ;
#8482=PLANE ( 'NONE',  #8995 ) ;
#8495=STYLED_ITEM ( 'NONE', ( #3643 ), #9343 ) ;
#8497=LINE ( 'NONE', #10855, #1818 ) ;
#8518=EDGE_LOOP ( 'NONE', ( #2081, #290, #9862, #7894 ) ) ;
#8527=ORIENTED_EDGE ( 'NONE', *, *, #12574, .F. ) ;
#8637=CARTESIAN_POINT ( 'NONE',  ( -31.74999999999995737, 3.061616997868383634E-16, -2.500000000000028422 ) ) ;
#8719=DIRECTION ( 'NONE',  ( 0.000000000000000000, 0.000000000000000000, 1.000000000000000000 ) ) ;
#8729=VECTOR ( 'NONE', #14217, 1000.000000000000114 ) ;
#8731=TOROIDAL_SURFACE ( 'NONE', #6786, 2.700000000000000622, 0.2000000000000000111 ) ;
#8758=CARTESIAN_POINT ( 'NONE',  ( 0.2500000000000002220, 4.898587196589412829E-16, -4.000000000000000000 ) ) ;
#8791=ORIENTED_EDGE ( 'NONE', *, *, #3620, .F. ) ;
#8795=EDGE_CURVE ( 'NONE', #13116, #8815, #6168, .T. ) ;
#8815=VERTEX_POINT ( 'NONE', #560 ) ;
#8818=DIRECTION ( 'NONE',  ( -1.000000000000000000, 0.000000000000000000, 0.000000000000000000 ) ) ;
#8828=AXIS2_PLACEMENT_3D ( 'NONE', #7096, #12745, #2265 ) ;
#8829=CIRCLE ( 'NONE', #10047, 4.250000000000000000 ) ;
#8858=CARTESIAN_POINT ( 'NONE',  ( 0.2500000000000002220, 0.000000000000000000, 0.000000000000000000 ) ) ;
#8875=DIRECTION ( 'NONE',  ( 0.000000000000000000, 0.000000000000000000, 1.000000000000000000 ) ) ;
#8893=CYLINDRICAL_SURFACE ( 'NONE', #121, 2.500000000000000444 ) ;
#8895=FACE_OUTER_BOUND ( 'NONE', #13038, .T. ) ;
#8915=ORIENTED_EDGE ( 'NONE', *, *, #3245, .T. ) ;
#8941=CARTESIAN_POINT ( 'NONE',  ( 2.500000000000002220, 6.938893903907228378E-15, 2.042000000000002036 ) ) ;
#8946=CARTESIAN_POINT ( 'NONE',  ( 5.000000000000007994, 0.000000000000000000, 4.250000000000028422 ) ) ;
#8960=DIRECTION ( 'NONE',  ( -1.000000000000000000, 0.000000000000000000, 0.000000000000000000 ) ) ;
#8992=ORIENTED_EDGE ( 'NONE', *, *, #2545, .F. ) ;
#8995=AXIS2_PLACEMENT_3D ( 'NONE', #13207, #9846, #8418 ) ;
#8998=DIRECTION ( 'NONE',  ( -1.000000000000000000, -0.000000000000000000, -0.000000000000000000 ) ) ;
#9003=CIRCLE ( 'NONE', #1491, 2.041999999999999815 ) ;
#9011=CARTESIAN_POINT ( 'NONE',  ( 2.500000000000002220, -1.178949249685222522, -2.042000000000002036 ) ) ;
#9026=VECTOR ( 'NONE', #715, 1000.000000000000114 ) ;
#9039=CARTESIAN_POINT ( 'NONE',  ( 5.000000000000006217, 3.306546357697854226E-16, 2.700000000000028155 ) ) ;
#9085=DIRECTION ( 'NONE',  ( 0.000000000000000000, -0.5000000000000008882, -0.8660254037844380415 ) ) ;
#9125=EDGE_CURVE ( 'NONE', #7240, #14819, #10491, .T. ) ;
#9136=CARTESIAN_POINT ( 'NONE',  ( 54.99999999999999289, 2.055000000000001492, 0.000000000000000000 ) ) ;
#9151=VERTEX_POINT ( 'NONE', #13291 ) ;
#9180=FILL_AREA_STYLE_COLOUR ( '', #4147 ) ;
#9190=LINE ( 'NONE', #9, #4383 ) ;
#9204=EDGE_CURVE ( 'NONE', #5057, #13764, #4956, .T. ) ;
#9220=AXIS2_PLACEMENT_3D ( 'NONE', #13665, #7890, #2123 ) ;
#9226=EDGE_CURVE ( 'NONE', #11082, #5022, #2196, .T. ) ;
#9242=ORIENTED_EDGE ( 'NONE', *, *, #9204, .F. ) ;
#9254=ADVANCED_FACE ( 'NONE', ( #10251 ), #2054, .T. ) ;
#9311=ADVANCED_FACE ( 'NONE', ( #3195 ), #7812, .F. ) ;
#9332=SURFACE_STYLE_USAGE ( .BOTH. , #14045 ) ;
#9333=AXIS2_PLACEMENT_3D ( 'NONE', #1160, #11493, #2588 ) ;
#9336=ORIENTED_EDGE ( 'NONE', *, *, #3245, .F. ) ;
#9343=MANIFOLD_SOLID_BREP ( 'Hex', #10854 ) ;
#9366=AXIS2_PLACEMENT_3D ( 'NONE', #6154, #3592, #10795 ) ;
#9368=DIRECTION ( 'NONE',  ( -1.000000000000000000, 0.000000000000000000, 0.000000000000000000 ) ) ;
#9399=( NAMED_UNIT ( * ) SI_UNIT ( $, .STERADIAN. ) SOLID_ANGLE_UNIT ( ) );
#9447=FILL_AREA_STYLE ('',( #13035 ) ) ;
#9467=LINE ( 'NONE', #4171, #5441 ) ;
#9507=CARTESIAN_POINT ( 'NONE',  ( 0.000000000000000000, 2.357898499370430834, 0.000000000000000000 ) ) ;
#9524=FACE_OUTER_BOUND ( 'NONE', #5792, .T. ) ;
#9536=ORIENTED_EDGE ( 'NONE', *, *, #485, .T. ) ;
#9546=ORIENTED_EDGE ( 'NONE', *, *, #7537, .T. ) ;
#9552=EDGE_CURVE ( 'NONE', #11288, #13630, #2650, .T. ) ;
#9573=CIRCLE ( 'NONE', #1825, 2.041999999999999815 ) ;
#9593=PRODUCT_DEFINITION ( 'UNKNOWN', '', #6773, #13177 ) ;
#9626=DIRECTION ( 'NONE',  ( 0.000000000000000000, 0.000000000000000000, 1.000000000000000000 ) ) ;
#9633=ADVANCED_FACE ( 'NONE', ( #10005 ), #1699, .T. ) ;
#9635=CARTESIAN_POINT ( 'NONE',  ( 2.500000000000002220, 1.178949249685208533, -2.042000000000002036 ) ) ;
#9663=SHAPE_DEFINITION_REPRESENTATION ( #13495, #8006 ) ;
#9665=STYLED_ITEM ( 'NONE', ( #427 ), #6552 ) ;
#9692=CIRCLE ( 'NONE', #3658, 4.250000000000000000 ) ;
#9747=VECTOR ( 'NONE', #8007, 1000.000000000000000 ) ;
#9752=AXIS2_PLACEMENT_3D ( 'NONE', #14024, #6792, #8020 ) ;
#9782=VECTOR ( 'NONE', #14207, 1000.000000000000114 ) ;
#9804=CARTESIAN_POINT ( 'NONE',  ( 2.500000000000002220, 0.000000000000000000, 0.000000000000000000 ) ) ;
#9846=DIRECTION ( 'NONE',  ( 1.000000000000000000, 0.000000000000000000, 0.000000000000000000 ) ) ;
#9851=AXIS2_PLACEMENT_3D ( 'NONE', #625, #12239, #2887 ) ;
#9859=CARTESIAN_POINT ( 'NONE',  ( -31.74999999999995737, 0.000000000000000000, -2.775557561562891351E-14 ) ) ;
#9862=ORIENTED_EDGE ( 'NONE', *, *, #14511, .T. ) ;
#9879=CYLINDRICAL_SURFACE ( 'NONE', #5868, 4.250000000000000000 ) ;
#9908=CONICAL_SURFACE ( 'NONE', #3371, 2.041999999999999815, 1.047197551196591858 ) ;
#9909=ORIENTED_EDGE ( 'NONE', *, *, #3385, .T. ) ;
#9992=DIRECTION ( 'NONE',  ( -1.000000000000000000, 0.000000000000000000, 0.000000000000000000 ) ) ;
#9993=ORIENTED_EDGE ( 'NONE', *, *, #6845, .F. ) ;
#10005=FACE_OUTER_BOUND ( 'NONE', #4230, .T. ) ;
#10024=CARTESIAN_POINT ( 'NONE',  ( 2.500000000000002220, -1.178949249685208533, 2.042000000000002036 ) ) ;
#10047=AXIS2_PLACEMENT_3D ( 'NONE', #635, #12876, #7603 ) ;
#10092=EDGE_CURVE ( 'NONE', #4050, #3015, #11786, .T. ) ;
#10130=DIRECTION ( 'NONE',  ( -1.000000000000000000, 0.000000000000000000, 0.000000000000000000 ) ) ;
#10143=VECTOR ( 'NONE', #1081, 1000.000000000000227 ) ;
#10145=DIRECTION ( 'NONE',  ( 0.000000000000000000, 1.000000000000000000, -1.471414886128460880E-15 ) ) ;
#10165=CARTESIAN_POINT ( 'NONE',  ( 2.500000000000002220, -2.357898499370437939, 0.000000000000000000 ) ) ;
#10185=VECTOR ( 'NONE', #1306, 1000.000000000000000 ) ;
#10229=EDGE_LOOP ( 'NONE', ( #5736, #1795, #5434, #11964, #11756 ) ) ;
#10247=PLANE ( 'NONE',  #1345 ) ;
#10250=ORIENTED_EDGE ( 'NONE', *, *, #5483, .T. ) ;
#10251=FACE_OUTER_BOUND ( 'NONE', #5004, .T. ) ;
#10274=CIRCLE ( 'NONE', #6371, 4.000000000000000000 ) ;
#10311=CYLINDRICAL_SURFACE ( 'NONE', #12557, 4.250000000000000000 ) ;
#10337=DIRECTION ( 'NONE',  ( 0.000000000000000000, -0.5000000000000008882, -0.8660254037844380415 ) ) ;
#10343=ADVANCED_FACE ( 'NONE', ( #2958 ), #8731, .F. ) ;
#10368=ADVANCED_FACE ( 'NONE', ( #6960, #12755 ), #1208, .T. ) ;
#10407=FACE_OUTER_BOUND ( 'NONE', #7166, .T. ) ;
#10436=CARTESIAN_POINT ( 'NONE',  ( 2.500000000000002220, 1.178949249685215417, 2.042000000000002036 ) ) ;
#10469=PLANE ( 'NONE',  #3165 ) ;
#10491=LINE ( 'NONE', #9635, #13885 ) ;
#10495=CIRCLE ( 'NONE', #6126, 2.041999999999999815 ) ;
#10497=CARTESIAN_POINT ( 'NONE',  ( 5.000000000000006217, 0.000000000000000000, -2.699999999999972644 ) ) ;
#10556=LINE ( 'NONE', #2584, #3260 ) ;
#10591=EDGE_LOOP ( 'NONE', ( #9993, #7190, #14149, #11777 ) ) ;
#10598=ORIENTED_EDGE ( 'NONE', *, *, #13578, .T. ) ;
#10652=( GEOMETRIC_REPRESENTATION_CONTEXT ( 3 ) GLOBAL_UNCERTAINTY_ASSIGNED_CONTEXT ( ( #12108 ) ) GLOBAL_UNIT_ASSIGNED_CONTEXT ( ( #12583, #2257, #1133 ) ) REPRESENTATION_CONTEXT ( 'NONE', 'WORKASPACE' ) );
#10671=CIRCLE ( 'NONE', #9220, 4.000000000000000000 ) ;
#10703=ADVANCED_FACE ( 'NONE', ( #4090 ), #5451, .T. ) ;
#10716=VECTOR ( 'NONE', #2473, 999.9999999999998863 ) ;
#10750=DIRECTION ( 'NONE',  ( 0.000000000000000000, 0.000000000000000000, -1.000000000000000000 ) ) ;
#10768=DIRECTION ( 'NONE',  ( 1.000000000000000000, 0.000000000000000000, 0.000000000000000000 ) ) ;
#10795=DIRECTION ( 'NONE',  ( 0.000000000000000000, 1.000000000000000000, -1.287488025362403787E-15 ) ) ;
#10809=CARTESIAN_POINT ( 'NONE',  ( 2.500000000000002220, -1.178949249685222522, -2.042000000000002036 ) ) ;
#10825=( NAMED_UNIT ( * ) SI_UNIT ( $, .STERADIAN. ) SOLID_ANGLE_UNIT ( ) );
#10827=CIRCLE ( 'NONE', #12289, 2.500000000000000444 ) ;
#10832=CARTESIAN_POINT ( 'NONE',  ( 0.2500000000000002220, 0.000000000000000000, 4.000000000000000000 ) ) ;
#10843=CARTESIAN_POINT ( 'NONE',  ( 0.000000000000000000, -1.178949249685208533, 2.042000000000002036 ) ) ;
#10845=EDGE_LOOP ( 'NONE', ( #8915, #13348 ) ) ;
#10854=CLOSED_SHELL ( 'NONE', ( #4693, #12334, #10343, #9633, #11037, #14339, #10368, #24, #6984, #6941, #5107, #13437, #7005, #10703, #11093, #1353, #14900, #9254, #2672, #8115, #11382, #12068, #2777, #13868, #12978, #9311, #8051 ) ) ;
#10855=CARTESIAN_POINT ( 'NONE',  ( -31.74999999999995737, 0.000000000000000000, 4.249999999999972466 ) ) ;
#10884=EDGE_CURVE ( 'NONE', #2594, #8099, #8829, .T. ) ;
#10886=DIRECTION ( 'NONE',  ( 0.000000000000000000, -1.224646799147353454E-16, 1.000000000000000000 ) ) ;
#10974=DIRECTION ( 'NONE',  ( 0.000000000000000000, 0.000000000000000000, 1.000000000000000000 ) ) ;
#10985=DIRECTION ( 'NONE',  ( 0.000000000000000000, -1.000000000000000000, 0.000000000000000000 ) ) ;
#11008=DIRECTION ( 'NONE',  ( 0.000000000000000000, 0.000000000000000000, -1.000000000000000000 ) ) ;
#11037=ADVANCED_FACE ( 'NONE', ( #4285 ), #8893, .T. ) ;
#11082=VERTEX_POINT ( 'NONE', #9039 ) ;
#11091=FACE_OUTER_BOUND ( 'NONE', #2243, .T. ) ;
#11093=ADVANCED_FACE ( 'NONE', ( #10407 ), #3736, .T. ) ;
#11121=ORIENTED_EDGE ( 'NONE', *, *, #7408, .F. ) ;
#11168=DIRECTION ( 'NONE',  ( 0.000000000000000000, 0.000000000000000000, -1.000000000000000000 ) ) ;
#11174=AXIS2_PLACEMENT_3D ( 'NONE', #10165, #6739, #5476 ) ;
#11223=AXIS2_PLACEMENT_3D ( 'NONE', #12045, #4821, #2543 ) ;
#11244=CARTESIAN_POINT ( 'NONE',  ( 2.500000000000002220, 2.357898499370430834, -6.938893903907228378E-15 ) ) ;
#11288=VERTEX_POINT ( 'NONE', #14429 ) ;
#11314=ORIENTED_EDGE ( 'NONE', *, *, #5838, .F. ) ;
#11318=EDGE_CURVE ( 'NONE', #8099, #11582, #8497, .T. ) ;
#11325=EDGE_CURVE ( 'NONE', #3015, #13764, #9573, .T. ) ;
#11361=EDGE_CURVE ( 'NONE', #11582, #8372, #6669, .T. ) ;
#11382=ADVANCED_FACE ( 'NONE', ( #3046 ), #10247, .F. ) ;
#11427=EDGE_CURVE ( 'NONE', #23, #11288, #2077, .T. ) ;
#11453=DIRECTION ( 'NONE',  ( -1.000000000000000000, 0.000000000000000000, 0.000000000000000000 ) ) ;
#11482=AXIS2_PLACEMENT_3D ( 'NONE', #2078, #95, #6694 ) ;
#11484=CARTESIAN_POINT ( 'NONE',  ( 2.500000000000002220, -1.178949249685208533, 2.042000000000002036 ) ) ;
#11493=DIRECTION ( 'NONE',  ( 0.000000000000000000, -0.8660254037844388186, -0.4999999999999998335 ) ) ;
#11525=VERTEX_POINT ( 'NONE', #7110 ) ;
#11552=ORIENTED_EDGE ( 'NONE', *, *, #3013, .F. ) ;
#11565=LINE ( 'NONE', #11484, #10143 ) ;
#11582=VERTEX_POINT ( 'NONE', #210 ) ;
#11594=EDGE_LOOP ( 'NONE', ( #13416, #307, #4662 ) ) ;
#11620=CARTESIAN_POINT ( 'NONE',  ( 0.000000000000000000, 0.000000000000000000, 0.000000000000000000 ) ) ;
#11626=( NAMED_UNIT ( * ) PLANE_ANGLE_UNIT ( ) SI_UNIT ( $, .RADIAN. ) );
#11632=ORIENTED_EDGE ( 'NONE', *, *, #12704, .F. ) ;
#11651=APPLICATION_CONTEXT ( 'automotive_design' ) ;
#11655=ORIENTED_EDGE ( 'NONE', *, *, #3752, .T. ) ;
#11668=LINE ( 'NONE', #265, #541 ) ;
#11756=ORIENTED_EDGE ( 'NONE', *, *, #7871, .T. ) ;
#11763=DIRECTION ( 'NONE',  ( -1.000000000000000000, 0.000000000000000000, 0.000000000000000000 ) ) ;
#11777=ORIENTED_EDGE ( 'NONE', *, *, #11361, .T. ) ;
#11784=DIRECTION ( 'NONE',  ( -1.000000000000000000, 0.000000000000000000, 0.000000000000000000 ) ) ;
#11786=LINE ( 'NONE', #161, #2924 ) ;
#11787=EDGE_CURVE ( 'NONE', #13020, #11806, #9467, .T. ) ;
#11806=VERTEX_POINT ( 'NONE', #14787 ) ;
#11811=VECTOR ( 'NONE', #9085, 1000.000000000000227 ) ;
#11864=AXIS2_PLACEMENT_3D ( 'NONE', #7732, #12310, #8719 ) ;
#11869=CARTESIAN_POINT ( 'NONE',  ( 2.500000000000002220, 2.357898499370430834, -6.938893903907228378E-15 ) ) ;
#11939=AXIS2_PLACEMENT_3D ( 'NONE', #2410, #1712, #6318 ) ;
#11940=DIRECTION ( 'NONE',  ( 0.000000000000000000, 0.000000000000000000, 1.000000000000000000 ) ) ;
#11947=ORIENTED_EDGE ( 'NONE', *, *, #694, .T. ) ;
#11964=ORIENTED_EDGE ( 'NONE', *, *, #1474, .T. ) ;
#11977=EDGE_CURVE ( 'NONE', #13764, #6523, #10495, .T. ) ;
#11981=CARTESIAN_POINT ( 'NONE',  ( 2.500000000000002220, 2.357898499370430834, -6.938893903907228378E-15 ) ) ;
#12045=CARTESIAN_POINT ( 'NONE',  ( 55.00000000000000711, 0.000000000000000000, 0.000000000000000000 ) ) ;
#12047=EDGE_CURVE ( 'NONE', #14464, #11082, #2987, .T. ) ;
#12056=ORIENTED_EDGE ( 'NONE', *, *, #6715, .F. ) ;
#12068=ADVANCED_FACE ( 'NONE', ( #9524 ), #13261, .F. ) ;
#12082=CARTESIAN_POINT ( 'NONE',  ( 2.500000000000002220, 1.178949249685208533, -2.042000000000002036 ) ) ;
#12108=UNCERTAINTY_MEASURE_WITH_UNIT (LENGTH_MEASURE( 1.000000000000000082E-05 ), #12583, 'distance_accuracy_value', 'NONE');
#12115=FACE_OUTER_BOUND ( 'NONE', #14255, .T. ) ;
#12128=VERTEX_POINT ( 'NONE', #277 ) ;
#12132=VECTOR ( 'NONE', #8422, 1000.000000000000000 ) ;
#12133=AXIS2_PLACEMENT_3D ( 'NONE', #9804, #14296, #13305 ) ;
#12148=ORIENTED_EDGE ( 'NONE', *, *, #5612, .F. ) ;
#12219=DIRECTION ( 'NONE',  ( -1.000000000000000000, 0.000000000000000000, 0.000000000000000000 ) ) ;
#12232=DIRECTION ( 'NONE',  ( -1.000000000000000000, 0.000000000000000000, 0.000000000000000000 ) ) ;
#12239=DIRECTION ( 'NONE',  ( 1.000000000000000000, 0.000000000000000000, 0.000000000000000000 ) ) ;
#12241=VERTEX_POINT ( 'NONE', #5208 ) ;
#12289=AXIS2_PLACEMENT_3D ( 'NONE', #3444, #6985, #4656 ) ;
#12306=UNCERTAINTY_MEASURE_WITH_UNIT (LENGTH_MEASURE( 1.000000000000000082E-05 ), #6967, 'distance_accuracy_value', 'NONE');
#12307=DIRECTION ( 'NONE',  ( 0.000000000000000000, 0.000000000000000000, -1.000000000000000000 ) ) ;
#12310=DIRECTION ( 'NONE',  ( -1.000000000000000000, 0.000000000000000000, 0.000000000000000000 ) ) ;
#12334=ADVANCED_FACE ( 'NONE', ( #7701 ), #570, .T. ) ;
#12351=ORIENTED_EDGE ( 'NONE', *, *, #9204, .T. ) ;
#12374=DIRECTION ( 'NONE',  ( 1.000000000000000000, 0.000000000000000000, 0.000000000000000000 ) ) ;
#12380=CARTESIAN_POINT ( 'NONE',  ( 5.000000000000004441, 0.000000000000000000, 2.775557561562891351E-14 ) ) ;
#12388=( GEOMETRIC_REPRESENTATION_CONTEXT ( 3 ) GLOBAL_UNCERTAINTY_ASSIGNED_CONTEXT ( ( #12306 ) ) GLOBAL_UNIT_ASSIGNED_CONTEXT ( ( #6967, #11626, #9399 ) ) REPRESENTATION_CONTEXT ( 'NONE', 'WORKASPACE' ) );
#12396=DIRECTION ( 'NONE',  ( 1.000000000000000000, -0.000000000000000000, -0.000000000000000000 ) ) ;
#12423=ORIENTED_EDGE ( 'NONE', *, *, #5612, .T. ) ;
#12506=EDGE_CURVE ( 'NONE', #2474, #7240, #3309, .T. ) ;
#12525=ORIENTED_EDGE ( 'NONE', *, *, #12047, .F. ) ;
#12540=EDGE_CURVE ( 'NONE', #13630, #5022, #89, .T. ) ;
#12557=AXIS2_PLACEMENT_3D ( 'NONE', #2113, #5530, #6654 ) ;
#12573=CARTESIAN_POINT ( 'NONE',  ( 2.500000000000002220, -1.178949249685208533, 2.042000000000002036 ) ) ;
#12574=EDGE_CURVE ( 'NONE', #8815, #11525, #6014, .T. ) ;
#12581=LINE ( 'NONE', #2961, #1950 ) ;
#12582=DIRECTION ( 'NONE',  ( -1.000000000000000000, 0.000000000000000000, 0.000000000000000000 ) ) ;
#12583=( LENGTH_UNIT ( ) NAMED_UNIT ( * ) SI_UNIT ( .MILLI., .METRE. ) );
#12641=DIRECTION ( 'NONE',  ( 0.000000000000000000, -0.5000000000000012212, -0.8660254037844380415 ) ) ;
#12653=ORIENTED_EDGE ( 'NONE', *, *, #2210, .T. ) ;
#12679=DIRECTION ( 'NONE',  ( 0.000000000000000000, 0.000000000000000000, 1.000000000000000000 ) ) ;
#12700=AXIS2_PLACEMENT_3D ( 'NONE', #6234, #4897, #8382 ) ;
#12704=EDGE_CURVE ( 'NONE', #628, #11806, #13531, .T. ) ;
#12738=CARTESIAN_POINT ( 'NONE',  ( 5.000000000000004441, 4.249999999999998224, 2.775557561562891351E-14 ) ) ;
#12745=DIRECTION ( 'NONE',  ( -1.000000000000000000, 0.000000000000000000, 0.000000000000000000 ) ) ;
#12755=FACE_OUTER_BOUND ( 'NONE', #14855, .T. ) ;
#12802=VERTEX_POINT ( 'NONE', #2839 ) ;
#12840=( GEOMETRIC_REPRESENTATION_CONTEXT ( 3 ) GLOBAL_UNCERTAINTY_ASSIGNED_CONTEXT ( ( #1636 ) ) GLOBAL_UNIT_ASSIGNED_CONTEXT ( ( #12959, #5885, #10825 ) ) REPRESENTATION_CONTEXT ( 'NONE', 'WORKASPACE' ) );
#12848=DIRECTION ( 'NONE',  ( 0.000000000000000000, 0.000000000000000000, 1.000000000000000000 ) ) ;
#12862=ORIENTED_EDGE ( 'NONE', *, *, #1074, .F. ) ;
#12876=DIRECTION ( 'NONE',  ( -1.000000000000000000, 0.000000000000000000, 0.000000000000000000 ) ) ;
#12878=FACE_OUTER_BOUND ( 'NONE', #4153, .T. ) ;
#12896=FACE_OUTER_BOUND ( 'NONE', #661, .T. ) ;
#12913=ORIENTED_EDGE ( 'NONE', *, *, #5473, .T. ) ;
#12959=( LENGTH_UNIT ( ) NAMED_UNIT ( * ) SI_UNIT ( .MILLI., .METRE. ) );
#12964=LINE ( 'NONE', #1422, #7385 ) ;
#12978=ADVANCED_FACE ( 'NONE', ( #14335 ), #8482, .F. ) ;
#13020=VERTEX_POINT ( 'NONE', #10843 ) ;
#13035=FILL_AREA_STYLE_COLOUR ( '', #2895 ) ;
#13038=EDGE_LOOP ( 'NONE', ( #3095, #13198, #14099, #3257 ) ) ;
#13067=CARTESIAN_POINT ( 'NONE',  ( 2.500000000000002220, 0.000000000000000000, 0.000000000000000000 ) ) ;
#13098=CIRCLE ( 'NONE', #13827, 4.250000000000000000 ) ;
#13116=VERTEX_POINT ( 'NONE', #14728 ) ;
#13177=PRODUCT_DEFINITION_CONTEXT ( 'detailed design', #11651, 'design' ) ;
#13193=VECTOR ( 'NONE', #12641, 999.9999999999998863 ) ;
#13198=ORIENTED_EDGE ( 'NONE', *, *, #6845, .T. ) ;
#13207=CARTESIAN_POINT ( 'NONE',  ( 2.500000000000002220, 2.357898499370430834, -6.938893903907228378E-15 ) ) ;
#13256=EDGE_CURVE ( 'NONE', #8372, #5320, #13356, .T. ) ;
#13261=PLANE ( 'NONE',  #14376 ) ;
#13291=CARTESIAN_POINT ( 'NONE',  ( 0.000000000000000000, 0.000000000000000000, 4.000000000000000000 ) ) ;
#13305=DIRECTION ( 'NONE',  ( 0.000000000000000000, 0.000000000000000000, 1.000000000000000000 ) ) ;
#13318=ORIENTED_EDGE ( 'NONE', *, *, #11427, .T. ) ;
#13334=ORIENTED_EDGE ( 'NONE', *, *, #8795, .F. ) ;
#13348=ORIENTED_EDGE ( 'NONE', *, *, #9226, .T. ) ;
#13356=CIRCLE ( 'NONE', #6791, 0.2500000000000002220 ) ;
#13370=FACE_OUTER_BOUND ( 'NONE', #10591, .T. ) ;
#13381=DIRECTION ( 'NONE',  ( 0.000000000000000000, 0.000000000000000000, 1.000000000000000000 ) ) ;
#13416=ORIENTED_EDGE ( 'NONE', *, *, #6715, .T. ) ;
#13429=VERTEX_POINT ( 'NONE', #4445 ) ;
#13437=ADVANCED_FACE ( 'NONE', ( #6764 ), #4522, .T. ) ;
#13443=AXIS2_PLACEMENT_3D ( 'NONE', #159, #11784, #9626 ) ;
#13445=DIRECTION ( 'NONE',  ( 0.000000000000000000, 0.000000000000000000, -1.000000000000000000 ) ) ;
#13489=ORIENTED_EDGE ( 'NONE', *, *, #14971, .T. ) ;
#13495=PRODUCT_DEFINITION_SHAPE ( 'NONE', 'NONE',  #9593 ) ;
#13501=ORIENTED_EDGE ( 'NONE', *, *, #9226, .F. ) ;
#13513=DIRECTION ( 'NONE',  ( 1.000000000000000000, 0.000000000000000000, 0.000000000000000000 ) ) ;
#13517=EDGE_CURVE ( 'NONE', #8108, #11288, #1322, .T. ) ;
#13531=LINE ( 'NONE', #14688, #4958 ) ;
#13578=EDGE_CURVE ( 'NONE', #14819, #14961, #9003, .T. ) ;
#13630=VERTEX_POINT ( 'NONE', #6665 ) ;
#13661=CARTESIAN_POINT ( 'NONE',  ( 5.200000000000006395, 0.000000000000000000, 2.775557561562891351E-14 ) ) ;
#13665=CARTESIAN_POINT ( 'NONE',  ( 0.000000000000000000, 0.000000000000000000, 0.000000000000000000 ) ) ;
#13718=ORIENTED_EDGE ( 'NONE', *, *, #11361, .F. ) ;
#13764=VERTEX_POINT ( 'NONE', #8941 ) ;
#13768=EDGE_CURVE ( 'NONE', #12241, #2474, #3492, .T. ) ;
#13779=DIRECTION ( 'NONE',  ( 1.000000000000000000, 0.000000000000000000, 0.000000000000000000 ) ) ;
#13787=CARTESIAN_POINT ( 'NONE',  ( 5.000000000000007994, 0.000000000000000000, 2.775557561562891351E-14 ) ) ;
#13820=FACE_OUTER_BOUND ( 'NONE', #10229, .T. ) ;
#13825=SURFACE_STYLE_FILL_AREA ( #5342 ) ;
#13827=AXIS2_PLACEMENT_3D ( 'NONE', #13787, #1864, #1929 ) ;
#13868=ADVANCED_FACE ( 'NONE', ( #12115 ), #2850, .F. ) ;
#13885=VECTOR ( 'NONE', #6072, 1000.000000000000000 ) ;
#14015=LINE ( 'NONE', #4819, #5249 ) ;
#14024=CARTESIAN_POINT ( 'NONE',  ( 5.200000000000006395, 3.306546357697854226E-16, 2.700000000000028155 ) ) ;
#14029=ORIENTED_EDGE ( 'NONE', *, *, #11977, .F. ) ;
#14034=EDGE_LOOP ( 'NONE', ( #975, #11632, #5161, #14544, #7003 ) ) ;
#14045=SURFACE_SIDE_STYLE ('',( #13825 ) ) ;
#14099=ORIENTED_EDGE ( 'NONE', *, *, #6517, .T. ) ;
#14149=ORIENTED_EDGE ( 'NONE', *, *, #11318, .T. ) ;
#14207=DIRECTION ( 'NONE',  ( 0.000000000000000000, 0.4999999999999995559, -0.8660254037844389297 ) ) ;
#14212=DIRECTION ( 'NONE',  ( 0.000000000000000000, -1.000000000000000000, 1.287488025362403787E-15 ) ) ;
#14217=DIRECTION ( 'NONE',  ( -0.5000000000000051070, 0.000000000000000000, 0.8660254037844355990 ) ) ;
#14222=DIRECTION ( 'NONE',  ( -1.000000000000000000, 0.000000000000000000, 0.000000000000000000 ) ) ;
#14255=EDGE_LOOP ( 'NONE', ( #9536, #6797, #14029 ) ) ;
#14258=ORIENTED_EDGE ( 'NONE', *, *, #13256, .F. ) ;
#14296=DIRECTION ( 'NONE',  ( -1.000000000000000000, 0.000000000000000000, 0.000000000000000000 ) ) ;
#14322=ORIENTED_EDGE ( 'NONE', *, *, #3895, .F. ) ;
#14335=FACE_OUTER_BOUND ( 'NONE', #4142, .T. ) ;
#14339=ADVANCED_FACE ( 'NONE', ( #8895 ), #9879, .T. ) ;
#14340=VECTOR ( 'NONE', #2240, 1000.000000000000114 ) ;
#14349=DIRECTION ( 'NONE',  ( 0.000000000000000000, 0.000000000000000000, 1.000000000000000000 ) ) ;
#14376=AXIS2_PLACEMENT_3D ( 'NONE', #11981, #1347, #10750 ) ;
#14429=CARTESIAN_POINT ( 'NONE',  ( 54.55500000000000682, 3.061616997868366378E-16, -2.500000000000000444 ) ) ;
#14464=VERTEX_POINT ( 'NONE', #6979 ) ;
#14472=CARTESIAN_POINT ( 'NONE',  ( 2.500000000000002220, 1.178949249685208533, -2.042000000000002036 ) ) ;
#14502=DIRECTION ( 'NONE',  ( 0.000000000000000000, 0.000000000000000000, 1.000000000000000000 ) ) ;
#14510=EDGE_CURVE ( 'NONE', #4050, #13020, #9190, .T. ) ;
#14511=EDGE_CURVE ( 'NONE', #23, #14464, #7907, .T. ) ;
#14534=ORIENTED_EDGE ( 'NONE', *, *, #12506, .F. ) ;
#14544=ORIENTED_EDGE ( 'NONE', *, *, #3385, .F. ) ;
#14575=DIRECTION ( 'NONE',  ( 0.000000000000000000, 0.000000000000000000, 1.000000000000000000 ) ) ;
#14581=EDGE_LOOP ( 'NONE', ( #1, #7953 ) ) ;
#14688=CARTESIAN_POINT ( 'NONE',  ( 2.500000000000002220, 1.178949249685215417, 2.042000000000002036 ) ) ;
#14728=CARTESIAN_POINT ( 'NONE',  ( 0.000000000000000000, 2.357898499370430834, 0.000000000000000000 ) ) ;
#14738=CARTESIAN_POINT ( 'NONE',  ( 54.55500000000000682, 0.000000000000000000, 0.000000000000000000 ) ) ;
#14787=CARTESIAN_POINT ( 'NONE',  ( 0.000000000000000000, 1.178949249685215417, 2.042000000000002036 ) ) ;
#14798=ORIENTED_EDGE ( 'NONE', *, *, #9125, .T. ) ;
#14812=PLANE ( 'NONE',  #973 ) ;
#14819=VERTEX_POINT ( 'NONE', #7664 ) ;
#14822=AXIS2_PLACEMENT_3D ( 'NONE', #11620, #4777, #3491 ) ;
#14853=ORIENTED_EDGE ( 'NONE', *, *, #5473, .F. ) ;
#14855=EDGE_LOOP ( 'NONE', ( #4520, #13489 ) ) ;
#14869=ORIENTED_EDGE ( 'NONE', *, *, #11325, .T. ) ;
#14891=DIRECTION ( 'NONE',  ( -1.000000000000000000, -0.000000000000000000, -0.000000000000000000 ) ) ;
#14900=ADVANCED_FACE ( 'NONE', ( #13820 ), #10469, .T. ) ;
#14902=LINE ( 'NONE', #1523, #9782 ) ;
#14932=AXIS2_PLACEMENT_3D ( 'NONE', #14738, #7729, #8875 ) ;
#14961=VERTEX_POINT ( 'NONE', #4415 ) ;
#14971=EDGE_CURVE ( 'NONE', #5320, #9151, #10671, .T. ) ;
#14982=LINE ( 'NONE', #4576, #8220 ) ;
ENDSEC;
END-ISO-10303-21;
